ISO-10303-21;
HEADER;
/* Generated by software containing ST-Developer
 * from STEP Tools, Inc. (www.steptools.com) 
 */

FILE_DESCRIPTION(
/* description */ ('Compact intermittent indexer'),
/* implementation_level */ '2;1');

FILE_NAME(
/* name */ 'M4x4 collar screw.step',
/* time_stamp */ '2026-10-29T16:32:17-07:00',
/* author */ (''),
/* organization */ (''),
/* preprocessor_version */ 'ST-DEVELOPER v20.2',
/* originating_system */ 'Autodesk Translation Framework v15.17.0.0',
/* authorisation */ '');

FILE_SCHEMA (('AUTOMOTIVE_DESIGN { 1 0 10303 214 3 1 1 }'));
ENDSEC;

DATA;
#10=MECHANICAL_DESIGN_GEOMETRIC_PRESENTATION_REPRESENTATION('',(#288),#10837);
#206=CONICAL_SURFACE('',#6646,0.185,0.785398163397449);
#232=SHAPE_REPRESENTATION_RELATIONSHIP('SRR','None',#10969,#256);
#256=ADVANCED_BREP_SHAPE_REPRESENTATION('',(#318),#10836);
#288=STYLED_ITEM('',(#11173),#318);
#318=MANIFOLD_SOLID_BREP('Body1',#5662);
#470=FACE_BOUND('',#1429,.T.);
#643=PLANE('',#6635);
#644=PLANE('',#6637);
#645=PLANE('',#6638);
#646=PLANE('',#6639);
#647=PLANE('',#6640);
#648=PLANE('',#6641);
#649=PLANE('',#6642);
#650=PLANE('',#6643);
#651=PLANE('',#6644);
#975=FACE_OUTER_BOUND('',#1420,.T.);
#976=FACE_OUTER_BOUND('',#1421,.T.);
#977=FACE_OUTER_BOUND('',#1422,.T.);
#978=FACE_OUTER_BOUND('',#1423,.T.);
#979=FACE_OUTER_BOUND('',#1424,.T.);
#980=FACE_OUTER_BOUND('',#1425,.T.);
#981=FACE_OUTER_BOUND('',#1426,.T.);
#982=FACE_OUTER_BOUND('',#1427,.T.);
#983=FACE_OUTER_BOUND('',#1428,.T.);
#984=FACE_OUTER_BOUND('',#1430,.T.);
#985=FACE_OUTER_BOUND('',#1431,.T.);
#1420=EDGE_LOOP('',(#5126));
#1421=EDGE_LOOP('',(#5127,#5128,#5129,#5130));
#1422=EDGE_LOOP('',(#5131,#5132,#5133,#5134));
#1423=EDGE_LOOP('',(#5135,#5136,#5137,#5138));
#1424=EDGE_LOOP('',(#5139,#5140,#5141,#5142));
#1425=EDGE_LOOP('',(#5143,#5144,#5145,#5146));
#1426=EDGE_LOOP('',(#5147,#5148,#5149,#5150));
#1427=EDGE_LOOP('',(#5151,#5152,#5153,#5154,#5155,#5156));
#1428=EDGE_LOOP('',(#5157));
#1429=EDGE_LOOP('',(#5158,#5159,#5160,#5161,#5162,#5163));
#1430=EDGE_LOOP('',(#5164,#5165,#5166,#5167));
#1431=EDGE_LOOP('',(#5168,#5169,#5170,#5171));
#1770=LINE('',#10718,#2128);
#1771=LINE('',#10720,#2129);
#1772=LINE('',#10722,#2130);
#1773=LINE('',#10723,#2131);
#1774=LINE('',#10726,#2132);
#1775=LINE('',#10728,#2133);
#1776=LINE('',#10729,#2134);
#1777=LINE('',#10732,#2135);
#1778=LINE('',#10734,#2136);
#1779=LINE('',#10735,#2137);
#1780=LINE('',#10738,#2138);
#1781=LINE('',#10740,#2139);
#1782=LINE('',#10741,#2140);
#1783=LINE('',#10744,#2141);
#1784=LINE('',#10746,#2142);
#1785=LINE('',#10747,#2143);
#1786=LINE('',#10749,#2144);
#1787=LINE('',#10750,#2145);
#1788=LINE('',#10758,#2146);
#1789=LINE('',#10760,#2147);
#2128=VECTOR('',#8424,1.);
#2129=VECTOR('',#8425,1.);
#2130=VECTOR('',#8426,1.);
#2131=VECTOR('',#8427,1.);
#2132=VECTOR('',#8430,1.);
#2133=VECTOR('',#8431,1.);
#2134=VECTOR('',#8432,1.);
#2135=VECTOR('',#8435,1.);
#2136=VECTOR('',#8436,1.);
#2137=VECTOR('',#8437,1.);
#2138=VECTOR('',#8440,1.);
#2139=VECTOR('',#8441,1.);
#2140=VECTOR('',#8442,1.);
#2141=VECTOR('',#8445,1.);
#2142=VECTOR('',#8446,1.);
#2143=VECTOR('',#8447,1.);
#2144=VECTOR('',#8450,1.);
#2145=VECTOR('',#8451,1.);
#2146=VECTOR('',#8462,0.185);
#2147=VECTOR('',#8465,0.2);
#2479=CIRCLE('',#6636,0.1954);
#2480=CIRCLE('',#6645,0.17);
#2481=CIRCLE('',#6647,0.1954);
#2961=VERTEX_POINT('',#10713);
#2962=VERTEX_POINT('',#10716);
#2963=VERTEX_POINT('',#10717);
#2964=VERTEX_POINT('',#10719);
#2965=VERTEX_POINT('',#10721);
#2966=VERTEX_POINT('',#10725);
#2967=VERTEX_POINT('',#10727);
#2968=VERTEX_POINT('',#10731);
#2969=VERTEX_POINT('',#10733);
#2970=VERTEX_POINT('',#10737);
#2971=VERTEX_POINT('',#10739);
#2972=VERTEX_POINT('',#10743);
#2973=VERTEX_POINT('',#10745);
#2974=VERTEX_POINT('',#10753);
#2975=VERTEX_POINT('',#10756);
#3685=EDGE_CURVE('',#2961,#2961,#2479,.T.);
#3686=EDGE_CURVE('',#2962,#2963,#1770,.T.);
#3687=EDGE_CURVE('',#2962,#2964,#1771,.T.);
#3688=EDGE_CURVE('',#2964,#2965,#1772,.T.);
#3689=EDGE_CURVE('',#2963,#2965,#1773,.T.);
#3690=EDGE_CURVE('',#2966,#2962,#1774,.T.);
#3691=EDGE_CURVE('',#2966,#2967,#1775,.T.);
#3692=EDGE_CURVE('',#2967,#2964,#1776,.T.);
#3693=EDGE_CURVE('',#2968,#2966,#1777,.T.);
#3694=EDGE_CURVE('',#2968,#2969,#1778,.T.);
#3695=EDGE_CURVE('',#2969,#2967,#1779,.T.);
#3696=EDGE_CURVE('',#2970,#2968,#1780,.T.);
#3697=EDGE_CURVE('',#2970,#2971,#1781,.T.);
#3698=EDGE_CURVE('',#2971,#2969,#1782,.T.);
#3699=EDGE_CURVE('',#2972,#2970,#1783,.T.);
#3700=EDGE_CURVE('',#2972,#2973,#1784,.T.);
#3701=EDGE_CURVE('',#2973,#2971,#1785,.T.);
#3702=EDGE_CURVE('',#2963,#2972,#1786,.T.);
#3703=EDGE_CURVE('',#2965,#2973,#1787,.T.);
#3704=EDGE_CURVE('',#2974,#2974,#2480,.T.);
#3705=EDGE_CURVE('',#2975,#2975,#2481,.T.);
#3706=EDGE_CURVE('',#2975,#2974,#1788,.T.);
#3707=EDGE_CURVE('',#2961,#2975,#1789,.T.);
#5126=ORIENTED_EDGE('',*,*,#3685,.F.);
#5127=ORIENTED_EDGE('',*,*,#3686,.F.);
#5128=ORIENTED_EDGE('',*,*,#3687,.T.);
#5129=ORIENTED_EDGE('',*,*,#3688,.T.);
#5130=ORIENTED_EDGE('',*,*,#3689,.F.);
#5131=ORIENTED_EDGE('',*,*,#3690,.F.);
#5132=ORIENTED_EDGE('',*,*,#3691,.T.);
#5133=ORIENTED_EDGE('',*,*,#3692,.T.);
#5134=ORIENTED_EDGE('',*,*,#3687,.F.);
#5135=ORIENTED_EDGE('',*,*,#3693,.F.);
#5136=ORIENTED_EDGE('',*,*,#3694,.T.);
#5137=ORIENTED_EDGE('',*,*,#3695,.T.);
#5138=ORIENTED_EDGE('',*,*,#3691,.F.);
#5139=ORIENTED_EDGE('',*,*,#3696,.F.);
#5140=ORIENTED_EDGE('',*,*,#3697,.T.);
#5141=ORIENTED_EDGE('',*,*,#3698,.T.);
#5142=ORIENTED_EDGE('',*,*,#3694,.F.);
#5143=ORIENTED_EDGE('',*,*,#3699,.F.);
#5144=ORIENTED_EDGE('',*,*,#3700,.T.);
#5145=ORIENTED_EDGE('',*,*,#3701,.T.);
#5146=ORIENTED_EDGE('',*,*,#3697,.F.);
#5147=ORIENTED_EDGE('',*,*,#3702,.F.);
#5148=ORIENTED_EDGE('',*,*,#3689,.T.);
#5149=ORIENTED_EDGE('',*,*,#3703,.T.);
#5150=ORIENTED_EDGE('',*,*,#3700,.F.);
#5151=ORIENTED_EDGE('',*,*,#3703,.F.);
#5152=ORIENTED_EDGE('',*,*,#3688,.F.);
#5153=ORIENTED_EDGE('',*,*,#3692,.F.);
#5154=ORIENTED_EDGE('',*,*,#3695,.F.);
#5155=ORIENTED_EDGE('',*,*,#3698,.F.);
#5156=ORIENTED_EDGE('',*,*,#3701,.F.);
#5157=ORIENTED_EDGE('',*,*,#3704,.F.);
#5158=ORIENTED_EDGE('',*,*,#3686,.T.);
#5159=ORIENTED_EDGE('',*,*,#3702,.T.);
#5160=ORIENTED_EDGE('',*,*,#3699,.T.);
#5161=ORIENTED_EDGE('',*,*,#3696,.T.);
#5162=ORIENTED_EDGE('',*,*,#3693,.T.);
#5163=ORIENTED_EDGE('',*,*,#3690,.T.);
#5164=ORIENTED_EDGE('',*,*,#3705,.F.);
#5165=ORIENTED_EDGE('',*,*,#3706,.T.);
#5166=ORIENTED_EDGE('',*,*,#3704,.T.);
#5167=ORIENTED_EDGE('',*,*,#3706,.F.);
#5168=ORIENTED_EDGE('',*,*,#3685,.T.);
#5169=ORIENTED_EDGE('',*,*,#3707,.T.);
#5170=ORIENTED_EDGE('',*,*,#3705,.T.);
#5171=ORIENTED_EDGE('',*,*,#3707,.F.);
#5294=CYLINDRICAL_SURFACE('',#6648,0.1954);
#5618=ADVANCED_FACE('',(#975),#643,.F.);
#5619=ADVANCED_FACE('',(#976),#644,.F.);
#5620=ADVANCED_FACE('',(#977),#645,.F.);
#5621=ADVANCED_FACE('',(#978),#646,.F.);
#5622=ADVANCED_FACE('',(#979),#647,.F.);
#5623=ADVANCED_FACE('',(#980),#648,.F.);
#5624=ADVANCED_FACE('',(#981),#649,.F.);
#5625=ADVANCED_FACE('',(#982),#650,.F.);
#5626=ADVANCED_FACE('',(#983,#470),#651,.T.);
#5627=ADVANCED_FACE('',(#984),#206,.T.);
#5628=ADVANCED_FACE('',(#985),#5294,.T.);
#5662=CLOSED_SHELL('',(#5618,#5619,#5620,#5621,#5622,#5623,#5624,#5625,
#5626,#5627,#5628));
#6634=AXIS2_PLACEMENT_3D('',#10711,#8416,#8417);
#6635=AXIS2_PLACEMENT_3D('',#10712,#8418,#8419);
#6636=AXIS2_PLACEMENT_3D('',#10714,#8420,#8421);
#6637=AXIS2_PLACEMENT_3D('',#10715,#8422,#8423);
#6638=AXIS2_PLACEMENT_3D('',#10724,#8428,#8429);
#6639=AXIS2_PLACEMENT_3D('',#10730,#8433,#8434);
#6640=AXIS2_PLACEMENT_3D('',#10736,#8438,#8439);
#6641=AXIS2_PLACEMENT_3D('',#10742,#8443,#8444);
#6642=AXIS2_PLACEMENT_3D('',#10748,#8448,#8449);
#6643=AXIS2_PLACEMENT_3D('',#10751,#8452,#8453);
#6644=AXIS2_PLACEMENT_3D('',#10752,#8454,#8455);
#6645=AXIS2_PLACEMENT_3D('',#10754,#8456,#8457);
#6646=AXIS2_PLACEMENT_3D('',#10755,#8458,#8459);
#6647=AXIS2_PLACEMENT_3D('',#10757,#8460,#8461);
#6648=AXIS2_PLACEMENT_3D('',#10759,#8463,#8464);
#8416=DIRECTION('axis',(0.,0.,1.));
#8417=DIRECTION('refdir',(1.,0.,0.));
#8418=DIRECTION('center_axis',(0.,1.,0.));
#8419=DIRECTION('ref_axis',(1.,0.,0.));
#8420=DIRECTION('center_axis',(0.,1.,0.));
#8421=DIRECTION('ref_axis',(1.,0.,0.));
#8422=DIRECTION('center_axis',(0.866025403784439,0.,-0.5));
#8423=DIRECTION('ref_axis',(0.5,0.,0.866025403784439));
#8424=DIRECTION('',(0.5,0.,0.866025403784439));
#8425=DIRECTION('',(0.,-1.,0.));
#8426=DIRECTION('',(0.5,0.,0.866025403784439));
#8427=DIRECTION('',(0.,-1.,0.));
#8428=DIRECTION('center_axis',(1.20185167898973E-16,0.,-1.));
#8429=DIRECTION('ref_axis',(1.,0.,1.20185167898973E-16));
#8430=DIRECTION('',(1.,0.,1.20185167898973E-16));
#8431=DIRECTION('',(0.,-1.,0.));
#8432=DIRECTION('',(1.,0.,1.20185167898973E-16));
#8433=DIRECTION('center_axis',(-0.866025403784439,0.,-0.5));
#8434=DIRECTION('ref_axis',(0.5,0.,-0.866025403784439));
#8435=DIRECTION('',(0.5,0.,-0.866025403784439));
#8436=DIRECTION('',(0.,-1.,0.));
#8437=DIRECTION('',(0.5,0.,-0.866025403784439));
#8438=DIRECTION('center_axis',(-0.866025403784439,0.,0.5));
#8439=DIRECTION('ref_axis',(-0.5,0.,-0.866025403784439));
#8440=DIRECTION('',(-0.5,0.,-0.866025403784439));
#8441=DIRECTION('',(0.,-1.,0.));
#8442=DIRECTION('',(-0.5,0.,-0.866025403784439));
#8443=DIRECTION('center_axis',(-2.40370335797945E-16,0.,1.));
#8444=DIRECTION('ref_axis',(-1.,0.,-2.40370335797945E-16));
#8445=DIRECTION('',(-1.,0.,-2.40370335797945E-16));
#8446=DIRECTION('',(0.,-1.,0.));
#8447=DIRECTION('',(-1.,0.,-2.40370335797945E-16));
#8448=DIRECTION('center_axis',(0.866025403784439,0.,0.5));
#8449=DIRECTION('ref_axis',(-0.5,0.,0.866025403784439));
#8450=DIRECTION('',(-0.5,0.,0.866025403784439));
#8451=DIRECTION('',(-0.5,0.,0.866025403784439));
#8452=DIRECTION('center_axis',(0.,-1.,0.));
#8453=DIRECTION('ref_axis',(0.,0.,-1.));
#8454=DIRECTION('center_axis',(0.,1.,0.));
#8455=DIRECTION('ref_axis',(0.,0.,1.));
#8456=DIRECTION('center_axis',(0.,-1.,0.));
#8457=DIRECTION('ref_axis',(1.,0.,0.));
#8458=DIRECTION('center_axis',(0.,-1.,0.));
#8459=DIRECTION('ref_axis',(1.,0.,0.));
#8460=DIRECTION('center_axis',(0.,-1.,0.));
#8461=DIRECTION('ref_axis',(1.,0.,0.));
#8462=DIRECTION('',(0.707106781186548,0.707106781186547,8.65956056235494E-17));
#8463=DIRECTION('center_axis',(0.,-1.,0.));
#8464=DIRECTION('ref_axis',(1.,0.,0.));
#8465=DIRECTION('',(0.,1.,0.));
#10711=CARTESIAN_POINT('',(0.,0.,0.));
#10712=CARTESIAN_POINT('Origin',(0.,-0.4,0.));
#10713=CARTESIAN_POINT('',(-0.1954,-0.4,2.39295984553393E-17));
#10714=CARTESIAN_POINT('Origin',(0.,-0.4,0.));
#10715=CARTESIAN_POINT('Origin',(0.0577350269189626,0.,-0.1));
#10716=CARTESIAN_POINT('',(0.0577350269189626,0.,-0.1));
#10717=CARTESIAN_POINT('',(0.115470053837925,0.,0.));
#10718=CARTESIAN_POINT('',(0.0934187836487032,0.,-0.0381939203391614));
#10719=CARTESIAN_POINT('',(0.0577350269189626,-0.2,-0.1));
#10720=CARTESIAN_POINT('',(0.0577350269189626,0.,-0.1));
#10721=CARTESIAN_POINT('',(0.115470053837925,-0.2,0.));
#10722=CARTESIAN_POINT('',(0.115470053837925,-0.2,0.));
#10723=CARTESIAN_POINT('',(0.115470053837925,0.,0.));
#10724=CARTESIAN_POINT('Origin',(-0.0577350269189626,0.,-0.1));
#10725=CARTESIAN_POINT('',(-0.0577350269189626,0.,-0.1));
#10726=CARTESIAN_POINT('',(0.0561324865405187,0.,-0.1));
#10727=CARTESIAN_POINT('',(-0.0577350269189626,-0.2,-0.1));
#10728=CARTESIAN_POINT('',(-0.0577350269189626,0.,-0.1));
#10729=CARTESIAN_POINT('',(0.0577350269189626,-0.2,-0.1));
#10730=CARTESIAN_POINT('Origin',(-0.115470053837925,0.,-1.38777878078145E-17));
#10731=CARTESIAN_POINT('',(-0.115470053837925,0.,-1.41410031829988E-17));
#10732=CARTESIAN_POINT('',(-0.0797862971081845,0.,-0.0618060796608387));
#10733=CARTESIAN_POINT('',(-0.115470053837925,-0.2,-1.38777878078145E-17));
#10734=CARTESIAN_POINT('',(-0.115470053837925,0.,-1.41410031829988E-17));
#10735=CARTESIAN_POINT('',(-0.0577350269189626,-0.2,-0.1));
#10736=CARTESIAN_POINT('Origin',(-0.0577350269189626,0.,0.1));
#10737=CARTESIAN_POINT('',(-0.0577350269189626,0.,0.1));
#10738=CARTESIAN_POINT('',(-0.0509187836487033,0.,0.111806079660839));
#10739=CARTESIAN_POINT('',(-0.0577350269189626,-0.2,0.1));
#10740=CARTESIAN_POINT('',(-0.0577350269189626,0.,0.1));
#10741=CARTESIAN_POINT('',(-0.115470053837925,-0.2,-1.41410031829988E-17));
#10742=CARTESIAN_POINT('Origin',(0.0577350269189626,0.,0.1));
#10743=CARTESIAN_POINT('',(0.0577350269189626,0.,0.1));
#10744=CARTESIAN_POINT('',(0.113867513459481,0.,0.1));
#10745=CARTESIAN_POINT('',(0.0577350269189626,-0.2,0.1));
#10746=CARTESIAN_POINT('',(0.0577350269189626,0.,0.1));
#10747=CARTESIAN_POINT('',(-0.0577350269189626,-0.2,0.1));
#10748=CARTESIAN_POINT('Origin',(0.115470053837925,0.,0.));
#10749=CARTESIAN_POINT('',(0.122286297108185,0.,-0.0118060796608386));
#10750=CARTESIAN_POINT('',(0.0577350269189626,-0.2,0.1));
#10751=CARTESIAN_POINT('Origin',(0.,-0.2,0.));
#10752=CARTESIAN_POINT('Origin',(0.17,0.,0.));
#10753=CARTESIAN_POINT('',(-0.17,-8.67361737988404E-18,-2.0818995585505E-17));
#10754=CARTESIAN_POINT('Origin',(0.,0.,0.));
#10755=CARTESIAN_POINT('Origin',(0.,-0.015,0.));
#10756=CARTESIAN_POINT('',(-0.1954,-0.0254,-2.39295984553393E-17));
#10757=CARTESIAN_POINT('Origin',(0.,-0.0254,0.));
#10758=CARTESIAN_POINT('',(-0.185,-0.015,-2.2655965784226E-17));
#10759=CARTESIAN_POINT('Origin',(0.,-0.2775,0.));
#10760=CARTESIAN_POINT('',(-0.1954,-0.2775,-2.39295984553393E-17));
#10806=UNCERTAINTY_MEASURE_WITH_UNIT(LENGTH_MEASURE(0.001),#10838,
'DISTANCE_ACCURACY_VALUE',
'Maximum model space distance between geometric entities at asserted c
onnectivities');
#10807=UNCERTAINTY_MEASURE_WITH_UNIT(LENGTH_MEASURE(0.001),#10838,
'DISTANCE_ACCURACY_VALUE',
'Maximum model space distance between geometric entities at asserted c
onnectivities');
#10836=(
GEOMETRIC_REPRESENTATION_CONTEXT(3)
GLOBAL_UNCERTAINTY_ASSIGNED_CONTEXT((#10806))
GLOBAL_UNIT_ASSIGNED_CONTEXT((#10838,#10840,#10841))
REPRESENTATION_CONTEXT('','3D')
);
#10837=(
GEOMETRIC_REPRESENTATION_CONTEXT(3)
GLOBAL_UNCERTAINTY_ASSIGNED_CONTEXT((#10807))
GLOBAL_UNIT_ASSIGNED_CONTEXT((#10838,#10840,#10841))
REPRESENTATION_CONTEXT('','3D')
);
#10838=(
LENGTH_UNIT()
NAMED_UNIT(*)
SI_UNIT(.CENTI.,.METRE.)
);
#10840=(
NAMED_UNIT(*)
PLANE_ANGLE_UNIT()
SI_UNIT($,.RADIAN.)
);
#10841=(
NAMED_UNIT(*)
SI_UNIT($,.STERADIAN.)
SOLID_ANGLE_UNIT()
);
#10870=SHAPE_DEFINITION_REPRESENTATION(#10923,#10969);
#10923=PRODUCT_DEFINITION_SHAPE('',$,#10999);
#10969=SHAPE_REPRESENTATION('',(#6634),#10836);
#10970=PRODUCT_DEFINITION_CONTEXT('part definition',#11059,'design');
#10999=PRODUCT_DEFINITION('M4x4 collar screw','M4x4 collar screw',#11028,
#10970);
#11028=PRODUCT_DEFINITION_FORMATION('',$,#11089);
#11059=APPLICATION_CONTEXT(
'Core Data for Automotive Mechanical Design Process');
#11060=PRODUCT_CONTEXT('part definition',#11059,'mechanical');
#11089=PRODUCT('M4x4 collar screw','M4x4 collar screw',
'M4x4 collar screw',(#11060));
#11167=COLOUR_RGB('Black',0.12,0.14,0.17);
#11168=FILL_AREA_STYLE_COLOUR('',#11167);
#11169=FILL_AREA_STYLE('',(#11168));
#11170=SURFACE_STYLE_FILL_AREA(#11169);
#11171=SURFACE_SIDE_STYLE('',(#11170));
#11172=SURFACE_STYLE_USAGE(.BOTH.,#11171);
#11173=PRESENTATION_STYLE_ASSIGNMENT((#11172));
ENDSEC;
END-ISO-10303-21;
